ISO-10303-21;
HEADER;
/* Generated by software containing ST-Developer
 * from STEP Tools, Inc. (www.steptools.com) 
 */

FILE_DESCRIPTION(
/* description */ ('Gear mesh backlash fixture'),
/* implementation_level */ '2;1');

FILE_NAME(
/* name */ 'M4x4 collar screw.step',
/* time_stamp */ '2026-10-28T03:26:00-07:00',
/* author */ (''),
/* organization */ (''),
/* preprocessor_version */ 'ST-DEVELOPER v20.2',
/* originating_system */ 'Autodesk Translation Framework v15.17.0.0',
/* authorisation */ '');

FILE_SCHEMA (('AUTOMOTIVE_DESIGN { 1 0 10303 214 3 1 1 }'));
ENDSEC;

DATA;
#10=MECHANICAL_DESIGN_GEOMETRIC_PRESENTATION_REPRESENTATION('',(#1078),#57900);
#776=CONICAL_SURFACE('',#15303,0.185,0.785398163397449);
#963=SHAPE_REPRESENTATION_RELATIONSHIP('SRR','None',#58164,#1013);
#1013=ADVANCED_BREP_SHAPE_REPRESENTATION('',(#1141),#57897);
#1078=STYLED_ITEM('',(#58472),#1141);
#1141=MANIFOLD_SOLID_BREP('Body1',#13640);
#1325=FACE_BOUND('',#3220,.T.);
#1628=PLANE('',#15292);
#1629=PLANE('',#15294);
#1630=PLANE('',#15295);
#1631=PLANE('',#15296);
#1632=PLANE('',#15297);
#1633=PLANE('',#15298);
#1634=PLANE('',#15299);
#1635=PLANE('',#15300);
#1636=PLANE('',#15301);
#2264=FACE_OUTER_BOUND('',#3211,.T.);
#2265=FACE_OUTER_BOUND('',#3212,.T.);
#2266=FACE_OUTER_BOUND('',#3213,.T.);
#2267=FACE_OUTER_BOUND('',#3214,.T.);
#2268=FACE_OUTER_BOUND('',#3215,.T.);
#2269=FACE_OUTER_BOUND('',#3216,.T.);
#2270=FACE_OUTER_BOUND('',#3217,.T.);
#2271=FACE_OUTER_BOUND('',#3218,.T.);
#2272=FACE_OUTER_BOUND('',#3219,.T.);
#2273=FACE_OUTER_BOUND('',#3221,.T.);
#2274=FACE_OUTER_BOUND('',#3222,.T.);
#3211=EDGE_LOOP('',(#11489));
#3212=EDGE_LOOP('',(#11490,#11491,#11492,#11493));
#3213=EDGE_LOOP('',(#11494,#11495,#11496,#11497));
#3214=EDGE_LOOP('',(#11498,#11499,#11500,#11501));
#3215=EDGE_LOOP('',(#11502,#11503,#11504,#11505));
#3216=EDGE_LOOP('',(#11506,#11507,#11508,#11509));
#3217=EDGE_LOOP('',(#11510,#11511,#11512,#11513));
#3218=EDGE_LOOP('',(#11514,#11515,#11516,#11517,#11518,#11519));
#3219=EDGE_LOOP('',(#11520));
#3220=EDGE_LOOP('',(#11521,#11522,#11523,#11524,#11525,#11526));
#3221=EDGE_LOOP('',(#11527,#11528,#11529,#11530));
#3222=EDGE_LOOP('',(#11531,#11532,#11533,#11534));
#4086=LINE('',#34045,#4975);
#4087=LINE('',#34047,#4976);
#4088=LINE('',#34049,#4977);
#4089=LINE('',#34050,#4978);
#4090=LINE('',#34053,#4979);
#4091=LINE('',#34055,#4980);
#4092=LINE('',#34056,#4981);
#4093=LINE('',#34059,#4982);
#4094=LINE('',#34061,#4983);
#4095=LINE('',#34062,#4984);
#4096=LINE('',#34065,#4985);
#4097=LINE('',#34067,#4986);
#4098=LINE('',#34068,#4987);
#4099=LINE('',#34071,#4988);
#4100=LINE('',#34073,#4989);
#4101=LINE('',#34074,#4990);
#4102=LINE('',#34076,#4991);
#4103=LINE('',#34077,#4992);
#4104=LINE('',#34085,#4993);
#4105=LINE('',#34087,#4994);
#4975=VECTOR('',#18453,1.);
#4976=VECTOR('',#18454,1.);
#4977=VECTOR('',#18455,1.);
#4978=VECTOR('',#18456,1.);
#4979=VECTOR('',#18459,1.);
#4980=VECTOR('',#18460,1.);
#4981=VECTOR('',#18461,1.);
#4982=VECTOR('',#18464,1.);
#4983=VECTOR('',#18465,1.);
#4984=VECTOR('',#18466,1.);
#4985=VECTOR('',#18469,1.);
#4986=VECTOR('',#18470,1.);
#4987=VECTOR('',#18471,1.);
#4988=VECTOR('',#18474,1.);
#4989=VECTOR('',#18475,1.);
#4990=VECTOR('',#18476,1.);
#4991=VECTOR('',#18479,1.);
#4992=VECTOR('',#18480,1.);
#4993=VECTOR('',#18491,0.185);
#4994=VECTOR('',#18494,0.2);
#5687=CIRCLE('',#15293,0.1954);
#5688=CIRCLE('',#15302,0.17);
#5689=CIRCLE('',#15304,0.1954);
#6662=VERTEX_POINT('',#34040);
#6663=VERTEX_POINT('',#34043);
#6664=VERTEX_POINT('',#34044);
#6665=VERTEX_POINT('',#34046);
#6666=VERTEX_POINT('',#34048);
#6667=VERTEX_POINT('',#34052);
#6668=VERTEX_POINT('',#34054);
#6669=VERTEX_POINT('',#34058);
#6670=VERTEX_POINT('',#34060);
#6671=VERTEX_POINT('',#34064);
#6672=VERTEX_POINT('',#34066);
#6673=VERTEX_POINT('',#34070);
#6674=VERTEX_POINT('',#34072);
#6675=VERTEX_POINT('',#34080);
#6676=VERTEX_POINT('',#34083);
#8331=EDGE_CURVE('',#6662,#6662,#5687,.T.);
#8332=EDGE_CURVE('',#6663,#6664,#4086,.T.);
#8333=EDGE_CURVE('',#6663,#6665,#4087,.T.);
#8334=EDGE_CURVE('',#6665,#6666,#4088,.T.);
#8335=EDGE_CURVE('',#6664,#6666,#4089,.T.);
#8336=EDGE_CURVE('',#6667,#6663,#4090,.T.);
#8337=EDGE_CURVE('',#6667,#6668,#4091,.T.);
#8338=EDGE_CURVE('',#6668,#6665,#4092,.T.);
#8339=EDGE_CURVE('',#6669,#6667,#4093,.T.);
#8340=EDGE_CURVE('',#6669,#6670,#4094,.T.);
#8341=EDGE_CURVE('',#6670,#6668,#4095,.T.);
#8342=EDGE_CURVE('',#6671,#6669,#4096,.T.);
#8343=EDGE_CURVE('',#6671,#6672,#4097,.T.);
#8344=EDGE_CURVE('',#6672,#6670,#4098,.T.);
#8345=EDGE_CURVE('',#6673,#6671,#4099,.T.);
#8346=EDGE_CURVE('',#6673,#6674,#4100,.T.);
#8347=EDGE_CURVE('',#6674,#6672,#4101,.T.);
#8348=EDGE_CURVE('',#6664,#6673,#4102,.T.);
#8349=EDGE_CURVE('',#6666,#6674,#4103,.T.);
#8350=EDGE_CURVE('',#6675,#6675,#5688,.T.);
#8351=EDGE_CURVE('',#6676,#6676,#5689,.T.);
#8352=EDGE_CURVE('',#6676,#6675,#4104,.T.);
#8353=EDGE_CURVE('',#6662,#6676,#4105,.T.);
#11489=ORIENTED_EDGE('',*,*,#8331,.F.);
#11490=ORIENTED_EDGE('',*,*,#8332,.F.);
#11491=ORIENTED_EDGE('',*,*,#8333,.T.);
#11492=ORIENTED_EDGE('',*,*,#8334,.T.);
#11493=ORIENTED_EDGE('',*,*,#8335,.F.);
#11494=ORIENTED_EDGE('',*,*,#8336,.F.);
#11495=ORIENTED_EDGE('',*,*,#8337,.T.);
#11496=ORIENTED_EDGE('',*,*,#8338,.T.);
#11497=ORIENTED_EDGE('',*,*,#8333,.F.);
#11498=ORIENTED_EDGE('',*,*,#8339,.F.);
#11499=ORIENTED_EDGE('',*,*,#8340,.T.);
#11500=ORIENTED_EDGE('',*,*,#8341,.T.);
#11501=ORIENTED_EDGE('',*,*,#8337,.F.);
#11502=ORIENTED_EDGE('',*,*,#8342,.F.);
#11503=ORIENTED_EDGE('',*,*,#8343,.T.);
#11504=ORIENTED_EDGE('',*,*,#8344,.T.);
#11505=ORIENTED_EDGE('',*,*,#8340,.F.);
#11506=ORIENTED_EDGE('',*,*,#8345,.F.);
#11507=ORIENTED_EDGE('',*,*,#8346,.T.);
#11508=ORIENTED_EDGE('',*,*,#8347,.T.);
#11509=ORIENTED_EDGE('',*,*,#8343,.F.);
#11510=ORIENTED_EDGE('',*,*,#8348,.F.);
#11511=ORIENTED_EDGE('',*,*,#8335,.T.);
#11512=ORIENTED_EDGE('',*,*,#8349,.T.);
#11513=ORIENTED_EDGE('',*,*,#8346,.F.);
#11514=ORIENTED_EDGE('',*,*,#8349,.F.);
#11515=ORIENTED_EDGE('',*,*,#8334,.F.);
#11516=ORIENTED_EDGE('',*,*,#8338,.F.);
#11517=ORIENTED_EDGE('',*,*,#8341,.F.);
#11518=ORIENTED_EDGE('',*,*,#8344,.F.);
#11519=ORIENTED_EDGE('',*,*,#8347,.F.);
#11520=ORIENTED_EDGE('',*,*,#8350,.F.);
#11521=ORIENTED_EDGE('',*,*,#8332,.T.);
#11522=ORIENTED_EDGE('',*,*,#8348,.T.);
#11523=ORIENTED_EDGE('',*,*,#8345,.T.);
#11524=ORIENTED_EDGE('',*,*,#8342,.T.);
#11525=ORIENTED_EDGE('',*,*,#8339,.T.);
#11526=ORIENTED_EDGE('',*,*,#8336,.T.);
#11527=ORIENTED_EDGE('',*,*,#8351,.F.);
#11528=ORIENTED_EDGE('',*,*,#8352,.T.);
#11529=ORIENTED_EDGE('',*,*,#8350,.T.);
#11530=ORIENTED_EDGE('',*,*,#8352,.F.);
#11531=ORIENTED_EDGE('',*,*,#8331,.T.);
#11532=ORIENTED_EDGE('',*,*,#8353,.T.);
#11533=ORIENTED_EDGE('',*,*,#8351,.T.);
#11534=ORIENTED_EDGE('',*,*,#8353,.F.);
#12766=CYLINDRICAL_SURFACE('',#15305,0.1954);
#13381=ADVANCED_FACE('',(#2264),#1628,.F.);
#13382=ADVANCED_FACE('',(#2265),#1629,.F.);
#13383=ADVANCED_FACE('',(#2266),#1630,.F.);
#13384=ADVANCED_FACE('',(#2267),#1631,.F.);
#13385=ADVANCED_FACE('',(#2268),#1632,.F.);
#13386=ADVANCED_FACE('',(#2269),#1633,.F.);
#13387=ADVANCED_FACE('',(#2270),#1634,.F.);
#13388=ADVANCED_FACE('',(#2271),#1635,.F.);
#13389=ADVANCED_FACE('',(#2272,#1325),#1636,.T.);
#13390=ADVANCED_FACE('',(#2273),#776,.T.);
#13391=ADVANCED_FACE('',(#2274),#12766,.T.);
#13640=CLOSED_SHELL('',(#13381,#13382,#13383,#13384,#13385,#13386,#13387,
#13388,#13389,#13390,#13391));
#15291=AXIS2_PLACEMENT_3D('',#34038,#18445,#18446);
#15292=AXIS2_PLACEMENT_3D('',#34039,#18447,#18448);
#15293=AXIS2_PLACEMENT_3D('',#34041,#18449,#18450);
#15294=AXIS2_PLACEMENT_3D('',#34042,#18451,#18452);
#15295=AXIS2_PLACEMENT_3D('',#34051,#18457,#18458);
#15296=AXIS2_PLACEMENT_3D('',#34057,#18462,#18463);
#15297=AXIS2_PLACEMENT_3D('',#34063,#18467,#18468);
#15298=AXIS2_PLACEMENT_3D('',#34069,#18472,#18473);
#15299=AXIS2_PLACEMENT_3D('',#34075,#18477,#18478);
#15300=AXIS2_PLACEMENT_3D('',#34078,#18481,#18482);
#15301=AXIS2_PLACEMENT_3D('',#34079,#18483,#18484);
#15302=AXIS2_PLACEMENT_3D('',#34081,#18485,#18486);
#15303=AXIS2_PLACEMENT_3D('',#34082,#18487,#18488);
#15304=AXIS2_PLACEMENT_3D('',#34084,#18489,#18490);
#15305=AXIS2_PLACEMENT_3D('',#34086,#18492,#18493);
#18445=DIRECTION('axis',(0.,0.,1.));
#18446=DIRECTION('refdir',(1.,0.,0.));
#18447=DIRECTION('center_axis',(0.,1.,0.));
#18448=DIRECTION('ref_axis',(1.,0.,0.));
#18449=DIRECTION('center_axis',(0.,1.,0.));
#18450=DIRECTION('ref_axis',(1.,0.,0.));
#18451=DIRECTION('center_axis',(0.866025403784439,0.,-0.5));
#18452=DIRECTION('ref_axis',(0.5,0.,0.866025403784439));
#18453=DIRECTION('',(0.5,0.,0.866025403784439));
#18454=DIRECTION('',(0.,-1.,0.));
#18455=DIRECTION('',(0.5,0.,0.866025403784439));
#18456=DIRECTION('',(0.,-1.,0.));
#18457=DIRECTION('center_axis',(1.20185167898973E-16,0.,-1.));
#18458=DIRECTION('ref_axis',(1.,0.,1.20185167898973E-16));
#18459=DIRECTION('',(1.,0.,1.20185167898973E-16));
#18460=DIRECTION('',(0.,-1.,0.));
#18461=DIRECTION('',(1.,0.,1.20185167898973E-16));
#18462=DIRECTION('center_axis',(-0.866025403784439,0.,-0.5));
#18463=DIRECTION('ref_axis',(0.5,0.,-0.866025403784439));
#18464=DIRECTION('',(0.5,0.,-0.866025403784439));
#18465=DIRECTION('',(0.,-1.,0.));
#18466=DIRECTION('',(0.5,0.,-0.866025403784439));
#18467=DIRECTION('center_axis',(-0.866025403784439,0.,0.5));
#18468=DIRECTION('ref_axis',(-0.5,0.,-0.866025403784439));
#18469=DIRECTION('',(-0.5,0.,-0.866025403784439));
#18470=DIRECTION('',(0.,-1.,0.));
#18471=DIRECTION('',(-0.5,0.,-0.866025403784439));
#18472=DIRECTION('center_axis',(-2.40370335797945E-16,0.,1.));
#18473=DIRECTION('ref_axis',(-1.,0.,-2.40370335797945E-16));
#18474=DIRECTION('',(-1.,0.,-2.40370335797945E-16));
#18475=DIRECTION('',(0.,-1.,0.));
#18476=DIRECTION('',(-1.,0.,-2.40370335797945E-16));
#18477=DIRECTION('center_axis',(0.866025403784439,0.,0.5));
#18478=DIRECTION('ref_axis',(-0.5,0.,0.866025403784439));
#18479=DIRECTION('',(-0.5,0.,0.866025403784439));
#18480=DIRECTION('',(-0.5,0.,0.866025403784439));
#18481=DIRECTION('center_axis',(0.,-1.,0.));
#18482=DIRECTION('ref_axis',(0.,0.,-1.));
#18483=DIRECTION('center_axis',(0.,1.,0.));
#18484=DIRECTION('ref_axis',(0.,0.,1.));
#18485=DIRECTION('center_axis',(0.,-1.,0.));
#18486=DIRECTION('ref_axis',(1.,0.,0.));
#18487=DIRECTION('center_axis',(0.,-1.,0.));
#18488=DIRECTION('ref_axis',(1.,0.,0.));
#18489=DIRECTION('center_axis',(0.,-1.,0.));
#18490=DIRECTION('ref_axis',(1.,0.,0.));
#18491=DIRECTION('',(0.707106781186548,0.707106781186547,8.65956056235494E-17));
#18492=DIRECTION('center_axis',(0.,-1.,0.));
#18493=DIRECTION('ref_axis',(1.,0.,0.));
#18494=DIRECTION('',(0.,1.,0.));
#34038=CARTESIAN_POINT('',(0.,0.,0.));
#34039=CARTESIAN_POINT('Origin',(0.,-0.4,0.));
#34040=CARTESIAN_POINT('',(-0.1954,-0.4,2.39295984553393E-17));
#34041=CARTESIAN_POINT('Origin',(0.,-0.4,0.));
#34042=CARTESIAN_POINT('Origin',(0.0577350269189626,0.,-0.1));
#34043=CARTESIAN_POINT('',(0.0577350269189626,0.,-0.1));
#34044=CARTESIAN_POINT('',(0.115470053837925,0.,0.));
#34045=CARTESIAN_POINT('',(0.0934187836487032,0.,-0.0381939203391614));
#34046=CARTESIAN_POINT('',(0.0577350269189626,-0.2,-0.1));
#34047=CARTESIAN_POINT('',(0.0577350269189626,0.,-0.1));
#34048=CARTESIAN_POINT('',(0.115470053837925,-0.2,0.));
#34049=CARTESIAN_POINT('',(0.115470053837925,-0.2,0.));
#34050=CARTESIAN_POINT('',(0.115470053837925,0.,0.));
#34051=CARTESIAN_POINT('Origin',(-0.0577350269189626,0.,-0.1));
#34052=CARTESIAN_POINT('',(-0.0577350269189626,0.,-0.1));
#34053=CARTESIAN_POINT('',(0.0561324865405187,0.,-0.1));
#34054=CARTESIAN_POINT('',(-0.0577350269189626,-0.2,-0.1));
#34055=CARTESIAN_POINT('',(-0.0577350269189626,0.,-0.1));
#34056=CARTESIAN_POINT('',(0.0577350269189626,-0.2,-0.1));
#34057=CARTESIAN_POINT('Origin',(-0.115470053837925,0.,-1.38777878078145E-17));
#34058=CARTESIAN_POINT('',(-0.115470053837925,0.,-1.41410031829988E-17));
#34059=CARTESIAN_POINT('',(-0.0797862971081845,0.,-0.0618060796608387));
#34060=CARTESIAN_POINT('',(-0.115470053837925,-0.2,-1.38777878078145E-17));
#34061=CARTESIAN_POINT('',(-0.115470053837925,0.,-1.41410031829988E-17));
#34062=CARTESIAN_POINT('',(-0.0577350269189626,-0.2,-0.1));
#34063=CARTESIAN_POINT('Origin',(-0.0577350269189626,0.,0.1));
#34064=CARTESIAN_POINT('',(-0.0577350269189626,0.,0.1));
#34065=CARTESIAN_POINT('',(-0.0509187836487033,0.,0.111806079660839));
#34066=CARTESIAN_POINT('',(-0.0577350269189626,-0.2,0.1));
#34067=CARTESIAN_POINT('',(-0.0577350269189626,0.,0.1));
#34068=CARTESIAN_POINT('',(-0.115470053837925,-0.2,-1.41410031829988E-17));
#34069=CARTESIAN_POINT('Origin',(0.0577350269189626,0.,0.1));
#34070=CARTESIAN_POINT('',(0.0577350269189626,0.,0.1));
#34071=CARTESIAN_POINT('',(0.113867513459481,0.,0.1));
#34072=CARTESIAN_POINT('',(0.0577350269189626,-0.2,0.1));
#34073=CARTESIAN_POINT('',(0.0577350269189626,0.,0.1));
#34074=CARTESIAN_POINT('',(-0.0577350269189626,-0.2,0.1));
#34075=CARTESIAN_POINT('Origin',(0.115470053837925,0.,0.));
#34076=CARTESIAN_POINT('',(0.122286297108185,0.,-0.0118060796608386));
#34077=CARTESIAN_POINT('',(0.0577350269189626,-0.2,0.1));
#34078=CARTESIAN_POINT('Origin',(0.,-0.2,0.));
#34079=CARTESIAN_POINT('Origin',(0.17,0.,0.));
#34080=CARTESIAN_POINT('',(-0.17,-8.67361737988404E-18,-2.0818995585505E-17));
#34081=CARTESIAN_POINT('Origin',(0.,0.,0.));
#34082=CARTESIAN_POINT('Origin',(0.,-0.015,0.));
#34083=CARTESIAN_POINT('',(-0.1954,-0.0254,-2.39295984553393E-17));
#34084=CARTESIAN_POINT('Origin',(0.,-0.0254,0.));
#34085=CARTESIAN_POINT('',(-0.185,-0.015,-2.2655965784226E-17));
#34086=CARTESIAN_POINT('Origin',(0.,-0.2775,0.));
#34087=CARTESIAN_POINT('',(-0.1954,-0.2775,-2.39295984553393E-17));
#57838=UNCERTAINTY_MEASURE_WITH_UNIT(LENGTH_MEASURE(0.001),#57901,
'DISTANCE_ACCURACY_VALUE',
'Maximum model space distance between geometric entities at asserted c
onnectivities');
#57841=UNCERTAINTY_MEASURE_WITH_UNIT(LENGTH_MEASURE(0.001),#57901,
'DISTANCE_ACCURACY_VALUE',
'Maximum model space distance between geometric entities at asserted c
onnectivities');
#57897=(
GEOMETRIC_REPRESENTATION_CONTEXT(3)
GLOBAL_UNCERTAINTY_ASSIGNED_CONTEXT((#57838))
GLOBAL_UNIT_ASSIGNED_CONTEXT((#57901,#57903,#57904))
REPRESENTATION_CONTEXT('','3D')
);
#57900=(
GEOMETRIC_REPRESENTATION_CONTEXT(3)
GLOBAL_UNCERTAINTY_ASSIGNED_CONTEXT((#57841))
GLOBAL_UNIT_ASSIGNED_CONTEXT((#57901,#57903,#57904))
REPRESENTATION_CONTEXT('','3D')
);
#57901=(
LENGTH_UNIT()
NAMED_UNIT(*)
SI_UNIT(.CENTI.,.METRE.)
);
#57903=(
NAMED_UNIT(*)
PLANE_ANGLE_UNIT()
SI_UNIT($,.RADIAN.)
);
#57904=(
NAMED_UNIT(*)
SI_UNIT($,.STERADIAN.)
SOLID_ANGLE_UNIT()
);
#57960=SHAPE_DEFINITION_REPRESENTATION(#58031,#58164);
#58031=PRODUCT_DEFINITION_SHAPE('',$,#58223);
#58164=SHAPE_REPRESENTATION('',(#15291),#57897);
#58167=PRODUCT_DEFINITION_CONTEXT('part definition',#58343,'design');
#58223=PRODUCT_DEFINITION('M4x4 collar screw','M4x4 collar screw',#58281,
#58167);
#58281=PRODUCT_DEFINITION_FORMATION('',$,#58400);
#58343=APPLICATION_CONTEXT(
'Core Data for Automotive Mechanical Design Process');
#58344=PRODUCT_CONTEXT('part definition',#58343,'mechanical');
#58400=PRODUCT('M4x4 collar screw','M4x4 collar screw',
'M4x4 collar screw',(#58344));
#58466=COLOUR_RGB('Black',0.12,0.14,0.17);
#58467=FILL_AREA_STYLE_COLOUR('',#58466);
#58468=FILL_AREA_STYLE('',(#58467));
#58469=SURFACE_STYLE_FILL_AREA(#58468);
#58470=SURFACE_SIDE_STYLE('',(#58469));
#58471=SURFACE_STYLE_USAGE(.BOTH.,#58470);
#58472=PRESENTATION_STYLE_ASSIGNMENT((#58471));
ENDSEC;
END-ISO-10303-21;
